ISO-10303-21;
HEADER;
/* Generated by software containing ST-Developer
 * from STEP Tools, Inc. (www.steptools.com) 
 */

FILE_DESCRIPTION(
/* description */ ('PAT-001'),
/* implementation_level */ '2;1');

FILE_NAME(
/* name */ 'Take-up screw bracket.step',
/* time_stamp */ '2026-10-29T17:07:15-07:00',
/* author */ (''),
/* organization */ (''),
/* preprocessor_version */ 'ST-DEVELOPER v20.2',
/* originating_system */ 'Autodesk Translation Framework v15.17.0.0',
/* authorisation */ '');

FILE_SCHEMA (('AUTOMOTIVE_DESIGN { 1 0 10303 214 3 1 1 }'));
ENDSEC;

DATA;
#10=MECHANICAL_DESIGN_GEOMETRIC_PRESENTATION_REPRESENTATION('',(#392),#9622);
#334=SHAPE_REPRESENTATION_RELATIONSHIP('SRR','None',#9758,#359);
#359=ADVANCED_BREP_SHAPE_REPRESENTATION('',(#425),#9607);
#392=STYLED_ITEM('',(#9969),#425);
#425=MANIFOLD_SOLID_BREP('Body1',#5217);
#467=FACE_BOUND('',#1147,.T.);
#468=FACE_BOUND('',#1149,.T.);
#469=FACE_BOUND('',#1154,.T.);
#470=FACE_BOUND('',#1156,.T.);
#576=PLANE('',#5749);
#577=PLANE('',#5750);
#578=PLANE('',#5751);
#579=PLANE('',#5752);
#580=PLANE('',#5753);
#581=PLANE('',#5754);
#582=PLANE('',#5755);
#583=PLANE('',#5756);
#817=FACE_OUTER_BOUND('',#1143,.T.);
#818=FACE_OUTER_BOUND('',#1144,.T.);
#819=FACE_OUTER_BOUND('',#1145,.T.);
#820=FACE_OUTER_BOUND('',#1146,.T.);
#821=FACE_OUTER_BOUND('',#1148,.T.);
#822=FACE_OUTER_BOUND('',#1150,.T.);
#823=FACE_OUTER_BOUND('',#1151,.T.);
#824=FACE_OUTER_BOUND('',#1152,.T.);
#825=FACE_OUTER_BOUND('',#1153,.T.);
#826=FACE_OUTER_BOUND('',#1155,.T.);
#1143=EDGE_LOOP('',(#3921,#3922,#3923,#3924));
#1144=EDGE_LOOP('',(#3925,#3926,#3927,#3928));
#1145=EDGE_LOOP('',(#3929,#3930,#3931,#3932));
#1146=EDGE_LOOP('',(#3933,#3934,#3935,#3936));
#1147=EDGE_LOOP('',(#3937));
#1148=EDGE_LOOP('',(#3938,#3939,#3940,#3941));
#1149=EDGE_LOOP('',(#3942));
#1150=EDGE_LOOP('',(#3943,#3944,#3945,#3946,#3947,#3948));
#1151=EDGE_LOOP('',(#3949,#3950,#3951,#3952,#3953,#3954));
#1152=EDGE_LOOP('',(#3955,#3956,#3957,#3958));
#1153=EDGE_LOOP('',(#3959,#3960,#3961,#3962));
#1154=EDGE_LOOP('',(#3963));
#1155=EDGE_LOOP('',(#3964,#3965,#3966,#3967));
#1156=EDGE_LOOP('',(#3968));
#1470=LINE('',#8518,#1875);
#1471=LINE('',#8524,#1876);
#1472=LINE('',#8529,#1877);
#1473=LINE('',#8531,#1878);
#1474=LINE('',#8533,#1879);
#1475=LINE('',#8534,#1880);
#1476=LINE('',#8538,#1881);
#1477=LINE('',#8539,#1882);
#1478=LINE('',#8540,#1883);
#1479=LINE('',#8543,#1884);
#1480=LINE('',#8545,#1885);
#1481=LINE('',#8546,#1886);
#1482=LINE('',#8549,#1887);
#1483=LINE('',#8551,#1888);
#1484=LINE('',#8552,#1889);
#1485=LINE('',#8555,#1890);
#1486=LINE('',#8557,#1891);
#1487=LINE('',#8558,#1892);
#1488=LINE('',#8560,#1893);
#1489=LINE('',#8562,#1894);
#1875=VECTOR('',#6651,0.275);
#1876=VECTOR('',#6658,0.34);
#1877=VECTOR('',#6663,1.);
#1878=VECTOR('',#6664,1.);
#1879=VECTOR('',#6665,1.);
#1880=VECTOR('',#6666,1.);
#1881=VECTOR('',#6669,1.);
#1882=VECTOR('',#6670,1.);
#1883=VECTOR('',#6671,1.);
#1884=VECTOR('',#6674,1.);
#1885=VECTOR('',#6675,1.);
#1886=VECTOR('',#6676,1.);
#1887=VECTOR('',#6679,1.);
#1888=VECTOR('',#6680,1.);
#1889=VECTOR('',#6681,1.);
#1890=VECTOR('',#6684,1.);
#1891=VECTOR('',#6685,1.);
#1892=VECTOR('',#6686,1.);
#1893=VECTOR('',#6689,1.);
#1894=VECTOR('',#6692,1.);
#2320=CIRCLE('',#5744,0.275);
#2321=CIRCLE('',#5745,0.275);
#2322=CIRCLE('',#5747,0.34);
#2323=CIRCLE('',#5748,0.34);
#2564=VERTEX_POINT('',#8515);
#2565=VERTEX_POINT('',#8517);
#2566=VERTEX_POINT('',#8521);
#2567=VERTEX_POINT('',#8523);
#2568=VERTEX_POINT('',#8527);
#2569=VERTEX_POINT('',#8528);
#2570=VERTEX_POINT('',#8530);
#2571=VERTEX_POINT('',#8532);
#2572=VERTEX_POINT('',#8536);
#2573=VERTEX_POINT('',#8537);
#2574=VERTEX_POINT('',#8542);
#2575=VERTEX_POINT('',#8544);
#2576=VERTEX_POINT('',#8548);
#2577=VERTEX_POINT('',#8550);
#2578=VERTEX_POINT('',#8554);
#2579=VERTEX_POINT('',#8556);
#3064=EDGE_CURVE('',#2564,#2564,#2320,.T.);
#3065=EDGE_CURVE('',#2564,#2565,#1470,.T.);
#3066=EDGE_CURVE('',#2565,#2565,#2321,.T.);
#3067=EDGE_CURVE('',#2566,#2566,#2322,.T.);
#3068=EDGE_CURVE('',#2566,#2567,#1471,.T.);
#3069=EDGE_CURVE('',#2567,#2567,#2323,.T.);
#3070=EDGE_CURVE('',#2568,#2569,#1472,.T.);
#3071=EDGE_CURVE('',#2569,#2570,#1473,.T.);
#3072=EDGE_CURVE('',#2571,#2570,#1474,.T.);
#3073=EDGE_CURVE('',#2568,#2571,#1475,.T.);
#3074=EDGE_CURVE('',#2572,#2573,#1476,.T.);
#3075=EDGE_CURVE('',#2572,#2571,#1477,.T.);
#3076=EDGE_CURVE('',#2570,#2573,#1478,.T.);
#3077=EDGE_CURVE('',#2573,#2574,#1479,.T.);
#3078=EDGE_CURVE('',#2574,#2575,#1480,.T.);
#3079=EDGE_CURVE('',#2575,#2572,#1481,.T.);
#3080=EDGE_CURVE('',#2576,#2569,#1482,.T.);
#3081=EDGE_CURVE('',#2576,#2577,#1483,.T.);
#3082=EDGE_CURVE('',#2577,#2574,#1484,.T.);
#3083=EDGE_CURVE('',#2578,#2575,#1485,.T.);
#3084=EDGE_CURVE('',#2578,#2579,#1486,.T.);
#3085=EDGE_CURVE('',#2579,#2568,#1487,.T.);
#3086=EDGE_CURVE('',#2577,#2578,#1488,.T.);
#3087=EDGE_CURVE('',#2579,#2576,#1489,.T.);
#3921=ORIENTED_EDGE('',*,*,#3064,.F.);
#3922=ORIENTED_EDGE('',*,*,#3065,.T.);
#3923=ORIENTED_EDGE('',*,*,#3066,.F.);
#3924=ORIENTED_EDGE('',*,*,#3065,.F.);
#3925=ORIENTED_EDGE('',*,*,#3067,.F.);
#3926=ORIENTED_EDGE('',*,*,#3068,.T.);
#3927=ORIENTED_EDGE('',*,*,#3069,.F.);
#3928=ORIENTED_EDGE('',*,*,#3068,.F.);
#3929=ORIENTED_EDGE('',*,*,#3070,.T.);
#3930=ORIENTED_EDGE('',*,*,#3071,.T.);
#3931=ORIENTED_EDGE('',*,*,#3072,.F.);
#3932=ORIENTED_EDGE('',*,*,#3073,.F.);
#3933=ORIENTED_EDGE('',*,*,#3074,.F.);
#3934=ORIENTED_EDGE('',*,*,#3075,.T.);
#3935=ORIENTED_EDGE('',*,*,#3072,.T.);
#3936=ORIENTED_EDGE('',*,*,#3076,.T.);
#3937=ORIENTED_EDGE('',*,*,#3069,.T.);
#3938=ORIENTED_EDGE('',*,*,#3074,.T.);
#3939=ORIENTED_EDGE('',*,*,#3077,.T.);
#3940=ORIENTED_EDGE('',*,*,#3078,.T.);
#3941=ORIENTED_EDGE('',*,*,#3079,.T.);
#3942=ORIENTED_EDGE('',*,*,#3066,.T.);
#3943=ORIENTED_EDGE('',*,*,#3080,.F.);
#3944=ORIENTED_EDGE('',*,*,#3081,.T.);
#3945=ORIENTED_EDGE('',*,*,#3082,.T.);
#3946=ORIENTED_EDGE('',*,*,#3077,.F.);
#3947=ORIENTED_EDGE('',*,*,#3076,.F.);
#3948=ORIENTED_EDGE('',*,*,#3071,.F.);
#3949=ORIENTED_EDGE('',*,*,#3079,.F.);
#3950=ORIENTED_EDGE('',*,*,#3083,.F.);
#3951=ORIENTED_EDGE('',*,*,#3084,.T.);
#3952=ORIENTED_EDGE('',*,*,#3085,.T.);
#3953=ORIENTED_EDGE('',*,*,#3073,.T.);
#3954=ORIENTED_EDGE('',*,*,#3075,.F.);
#3955=ORIENTED_EDGE('',*,*,#3086,.T.);
#3956=ORIENTED_EDGE('',*,*,#3083,.T.);
#3957=ORIENTED_EDGE('',*,*,#3078,.F.);
#3958=ORIENTED_EDGE('',*,*,#3082,.F.);
#3959=ORIENTED_EDGE('',*,*,#3085,.F.);
#3960=ORIENTED_EDGE('',*,*,#3087,.T.);
#3961=ORIENTED_EDGE('',*,*,#3080,.T.);
#3962=ORIENTED_EDGE('',*,*,#3070,.F.);
#3963=ORIENTED_EDGE('',*,*,#3067,.T.);
#3964=ORIENTED_EDGE('',*,*,#3087,.F.);
#3965=ORIENTED_EDGE('',*,*,#3084,.F.);
#3966=ORIENTED_EDGE('',*,*,#3086,.F.);
#3967=ORIENTED_EDGE('',*,*,#3081,.F.);
#3968=ORIENTED_EDGE('',*,*,#3064,.T.);
#4859=CYLINDRICAL_SURFACE('',#5743,0.275);
#4860=CYLINDRICAL_SURFACE('',#5746,0.34);
#5004=ADVANCED_FACE('',(#817),#4859,.F.);
#5005=ADVANCED_FACE('',(#818),#4860,.F.);
#5006=ADVANCED_FACE('',(#819),#576,.T.);
#5007=ADVANCED_FACE('',(#820,#467),#577,.T.);
#5008=ADVANCED_FACE('',(#821,#468),#578,.T.);
#5009=ADVANCED_FACE('',(#822),#579,.T.);
#5010=ADVANCED_FACE('',(#823),#580,.T.);
#5011=ADVANCED_FACE('',(#824),#581,.T.);
#5012=ADVANCED_FACE('',(#825,#469),#582,.T.);
#5013=ADVANCED_FACE('',(#826,#470),#583,.F.);
#5217=CLOSED_SHELL('',(#5004,#5005,#5006,#5007,#5008,#5009,#5010,#5011,
#5012,#5013));
#5742=AXIS2_PLACEMENT_3D('',#8513,#6645,#6646);
#5743=AXIS2_PLACEMENT_3D('',#8514,#6647,#6648);
#5744=AXIS2_PLACEMENT_3D('',#8516,#6649,#6650);
#5745=AXIS2_PLACEMENT_3D('',#8519,#6652,#6653);
#5746=AXIS2_PLACEMENT_3D('',#8520,#6654,#6655);
#5747=AXIS2_PLACEMENT_3D('',#8522,#6656,#6657);
#5748=AXIS2_PLACEMENT_3D('',#8525,#6659,#6660);
#5749=AXIS2_PLACEMENT_3D('',#8526,#6661,#6662);
#5750=AXIS2_PLACEMENT_3D('',#8535,#6667,#6668);
#5751=AXIS2_PLACEMENT_3D('',#8541,#6672,#6673);
#5752=AXIS2_PLACEMENT_3D('',#8547,#6677,#6678);
#5753=AXIS2_PLACEMENT_3D('',#8553,#6682,#6683);
#5754=AXIS2_PLACEMENT_3D('',#8559,#6687,#6688);
#5755=AXIS2_PLACEMENT_3D('',#8561,#6690,#6691);
#5756=AXIS2_PLACEMENT_3D('',#8563,#6693,#6694);
#6645=DIRECTION('axis',(0.,0.,1.));
#6646=DIRECTION('refdir',(1.,0.,0.));
#6647=DIRECTION('center_axis',(0.,0.,1.));
#6648=DIRECTION('ref_axis',(1.,0.,0.));
#6649=DIRECTION('center_axis',(0.,0.,1.));
#6650=DIRECTION('ref_axis',(1.,0.,0.));
#6651=DIRECTION('',(0.,0.,1.));
#6652=DIRECTION('center_axis',(0.,0.,-1.));
#6653=DIRECTION('ref_axis',(1.,0.,0.));
#6654=DIRECTION('center_axis',(1.,0.,0.));
#6655=DIRECTION('ref_axis',(0.,0.,-1.));
#6656=DIRECTION('center_axis',(1.,0.,0.));
#6657=DIRECTION('ref_axis',(0.,0.,-1.));
#6658=DIRECTION('',(1.,0.,0.));
#6659=DIRECTION('center_axis',(-1.,0.,0.));
#6660=DIRECTION('ref_axis',(0.,0.,-1.));
#6661=DIRECTION('center_axis',(0.,0.,1.));
#6662=DIRECTION('ref_axis',(0.,-1.,0.));
#6663=DIRECTION('',(0.,-1.,0.));
#6664=DIRECTION('',(1.,0.,0.));
#6665=DIRECTION('',(0.,-1.,0.));
#6666=DIRECTION('',(1.,0.,0.));
#6667=DIRECTION('center_axis',(1.,0.,0.));
#6668=DIRECTION('ref_axis',(0.,0.,-1.));
#6669=DIRECTION('',(0.,-1.,0.));
#6670=DIRECTION('',(0.,0.,1.));
#6671=DIRECTION('',(0.,0.,-1.));
#6672=DIRECTION('center_axis',(0.,0.,1.));
#6673=DIRECTION('ref_axis',(1.,0.,0.));
#6674=DIRECTION('',(1.,0.,0.));
#6675=DIRECTION('',(0.,1.,0.));
#6676=DIRECTION('',(-1.,0.,0.));
#6677=DIRECTION('center_axis',(0.,-1.,0.));
#6678=DIRECTION('ref_axis',(1.,0.,0.));
#6679=DIRECTION('',(0.,0.,1.));
#6680=DIRECTION('',(1.,0.,0.));
#6681=DIRECTION('',(0.,0.,1.));
#6682=DIRECTION('center_axis',(0.,1.,0.));
#6683=DIRECTION('ref_axis',(-1.,0.,0.));
#6684=DIRECTION('',(0.,0.,1.));
#6685=DIRECTION('',(-1.,0.,0.));
#6686=DIRECTION('',(0.,0.,1.));
#6687=DIRECTION('center_axis',(1.,0.,0.));
#6688=DIRECTION('ref_axis',(0.,1.,0.));
#6689=DIRECTION('',(0.,1.,0.));
#6690=DIRECTION('center_axis',(-1.,0.,0.));
#6691=DIRECTION('ref_axis',(0.,-1.,0.));
#6692=DIRECTION('',(0.,-1.,0.));
#6693=DIRECTION('center_axis',(0.,0.,1.));
#6694=DIRECTION('ref_axis',(1.,0.,0.));
#8513=CARTESIAN_POINT('',(0.,0.,0.));
#8514=CARTESIAN_POINT('Origin',(-3.5,-2.,1.9));
#8515=CARTESIAN_POINT('',(-3.775,-2.,2.));
#8516=CARTESIAN_POINT('Origin',(-3.5,-2.,2.));
#8517=CARTESIAN_POINT('',(-3.775,-2.,2.8));
#8518=CARTESIAN_POINT('',(-3.775,-2.,1.9));
#8519=CARTESIAN_POINT('Origin',(-3.5,-2.,2.8));
#8520=CARTESIAN_POINT('Origin',(-5.1,-2.,4.5));
#8521=CARTESIAN_POINT('',(-5.,-2.,4.84));
#8522=CARTESIAN_POINT('Origin',(-5.,-2.,4.5));
#8523=CARTESIAN_POINT('',(-4.2,-2.,4.84));
#8524=CARTESIAN_POINT('',(-5.1,-2.,4.84));
#8525=CARTESIAN_POINT('Origin',(-4.2,-2.,4.5));
#8526=CARTESIAN_POINT('Origin',(-5.,-0.8,5.5));
#8527=CARTESIAN_POINT('',(-5.,-0.8,5.5));
#8528=CARTESIAN_POINT('',(-5.,-3.2,5.5));
#8529=CARTESIAN_POINT('',(-5.,-0.8,5.5));
#8530=CARTESIAN_POINT('',(-4.2,-3.2,5.5));
#8531=CARTESIAN_POINT('',(-5.,-3.2,5.5));
#8532=CARTESIAN_POINT('',(-4.2,-0.8,5.5));
#8533=CARTESIAN_POINT('',(-4.2,-0.8,5.5));
#8534=CARTESIAN_POINT('',(-5.,-0.8,5.5));
#8535=CARTESIAN_POINT('Origin',(-4.2,-2.,4.1));
#8536=CARTESIAN_POINT('',(-4.2,-0.8,2.8));
#8537=CARTESIAN_POINT('',(-4.2,-3.2,2.8));
#8538=CARTESIAN_POINT('',(-4.2,-2.,2.8));
#8539=CARTESIAN_POINT('',(-4.2,-0.8,2.7));
#8540=CARTESIAN_POINT('',(-4.2,-3.2,5.5));
#8541=CARTESIAN_POINT('Origin',(-4.,-2.,2.8));
#8542=CARTESIAN_POINT('',(-3.,-3.2,2.8));
#8543=CARTESIAN_POINT('',(-5.,-3.2,2.8));
#8544=CARTESIAN_POINT('',(-3.,-0.8,2.8));
#8545=CARTESIAN_POINT('',(-3.,-3.2,2.8));
#8546=CARTESIAN_POINT('',(-3.,-0.8,2.8));
#8547=CARTESIAN_POINT('Origin',(-5.,-3.2,2.));
#8548=CARTESIAN_POINT('',(-5.,-3.2,2.));
#8549=CARTESIAN_POINT('',(-5.,-3.2,2.));
#8550=CARTESIAN_POINT('',(-3.,-3.2,2.));
#8551=CARTESIAN_POINT('',(-5.,-3.2,2.));
#8552=CARTESIAN_POINT('',(-3.,-3.2,2.));
#8553=CARTESIAN_POINT('Origin',(-3.,-0.8,2.));
#8554=CARTESIAN_POINT('',(-3.,-0.8,2.));
#8555=CARTESIAN_POINT('',(-3.,-0.8,2.));
#8556=CARTESIAN_POINT('',(-5.,-0.8,2.));
#8557=CARTESIAN_POINT('',(-3.,-0.8,2.));
#8558=CARTESIAN_POINT('',(-5.,-0.8,2.));
#8559=CARTESIAN_POINT('Origin',(-3.,-3.2,2.));
#8560=CARTESIAN_POINT('',(-3.,-3.2,2.));
#8561=CARTESIAN_POINT('Origin',(-5.,-0.8,2.));
#8562=CARTESIAN_POINT('',(-5.,-0.8,2.));
#8563=CARTESIAN_POINT('Origin',(-4.,-2.,2.));
#9577=UNCERTAINTY_MEASURE_WITH_UNIT(LENGTH_MEASURE(0.001),#9623,
'DISTANCE_ACCURACY_VALUE',
'Maximum model space distance between geometric entities at asserted c
onnectivities');
#9592=UNCERTAINTY_MEASURE_WITH_UNIT(LENGTH_MEASURE(0.001),#9623,
'DISTANCE_ACCURACY_VALUE',
'Maximum model space distance between geometric entities at asserted c
onnectivities');
#9607=(
GEOMETRIC_REPRESENTATION_CONTEXT(3)
GLOBAL_UNCERTAINTY_ASSIGNED_CONTEXT((#9577))
GLOBAL_UNIT_ASSIGNED_CONTEXT((#9623,#9625,#9626))
REPRESENTATION_CONTEXT('','3D')
);
#9622=(
GEOMETRIC_REPRESENTATION_CONTEXT(3)
GLOBAL_UNCERTAINTY_ASSIGNED_CONTEXT((#9592))
GLOBAL_UNIT_ASSIGNED_CONTEXT((#9623,#9625,#9626))
REPRESENTATION_CONTEXT('','3D')
);
#9623=(
LENGTH_UNIT()
NAMED_UNIT(*)
SI_UNIT(.CENTI.,.METRE.)
);
#9625=(
NAMED_UNIT(*)
PLANE_ANGLE_UNIT()
SI_UNIT($,.RADIAN.)
);
#9626=(
NAMED_UNIT(*)
SI_UNIT($,.STERADIAN.)
SOLID_ANGLE_UNIT()
);
#9641=SHAPE_DEFINITION_REPRESENTATION(#9675,#9758);
#9675=PRODUCT_DEFINITION_SHAPE('',$,#9788);
#9758=SHAPE_REPRESENTATION('',(#5742),#9607);
#9773=PRODUCT_DEFINITION_CONTEXT('part definition',#9862,'design');
#9788=PRODUCT_DEFINITION('Take-up screw bracket',
'Take-up screw bracket',#9817,#9773);
#9817=PRODUCT_DEFINITION_FORMATION('',$,#9878);
#9862=APPLICATION_CONTEXT(
'Core Data for Automotive Mechanical Design Process');
#9863=PRODUCT_CONTEXT('part definition',#9862,'mechanical');
#9878=PRODUCT('Take-up screw bracket','Take-up screw bracket',
'Take-up screw bracket',(#9863));
#9963=COLOUR_RGB('Black',0.12,0.14,0.17);
#9964=FILL_AREA_STYLE_COLOUR('',#9963);
#9965=FILL_AREA_STYLE('',(#9964));
#9966=SURFACE_STYLE_FILL_AREA(#9965);
#9967=SURFACE_SIDE_STYLE('',(#9966));
#9968=SURFACE_STYLE_USAGE(.BOTH.,#9967);
#9969=PRESENTATION_STYLE_ASSIGNMENT((#9968));
ENDSEC;
END-ISO-10303-21;
